ISO-10303-21;
HEADER;
/* Generated by software containing ST-Developer
 * from STEP Tools, Inc. (www.steptools.com) 
 */

FILE_DESCRIPTION(
/* description */ (''),
/* implementation_level */ '2;1');

FILE_NAME(
/* name */ '15_DIN_471_25x1.2_Retaining_Ring.step',
/* time_stamp */ '2026-10-23T00:52:27+05:00',
/* author */ (''),
/* organization */ (''),
/* preprocessor_version */ 'ST-DEVELOPER v20.2',
/* originating_system */ 'Autodesk Translation Framework v15.15.0.0',
/* authorisation */ '');

FILE_SCHEMA (('AUTOMOTIVE_DESIGN { 1 0 10303 214 3 1 1 }'));
ENDSEC;

DATA;
#10=MECHANICAL_DESIGN_GEOMETRIC_PRESENTATION_REPRESENTATION('',(#1572),#59204);
#1525=SHAPE_REPRESENTATION_RELATIONSHIP('SRR','None',#59314,#1545);
#1545=ADVANCED_BREP_SHAPE_REPRESENTATION('',(#1592),#59201);
#1572=STYLED_ITEM('',(#59600),#1592);
#1592=MANIFOLD_SOLID_BREP('Retaining ring',#22821);
#1798=FACE_BOUND('',#5206,.T.);
#1799=FACE_BOUND('',#5207,.T.);
#1800=FACE_BOUND('',#5209,.T.);
#1801=FACE_BOUND('',#5210,.T.);
#2232=PLANE('',#24643);
#2233=PLANE('',#24647);
#2234=PLANE('',#24651);
#2235=PLANE('',#24655);
#2236=PLANE('',#24659);
#2237=PLANE('',#24660);
#2583=CYLINDRICAL_SURFACE('',#24637,0.1);
#2584=CYLINDRICAL_SURFACE('',#24640,0.1);
#2585=CYLINDRICAL_SURFACE('',#24644,0.328820889047374);
#2586=CYLINDRICAL_SURFACE('',#24648,1.195);
#2587=CYLINDRICAL_SURFACE('',#24652,0.328820889047374);
#2588=CYLINDRICAL_SURFACE('',#24656,1.53);
#3691=FACE_OUTER_BOUND('',#5195,.T.);
#3692=FACE_OUTER_BOUND('',#5196,.T.);
#3693=FACE_OUTER_BOUND('',#5197,.T.);
#3694=FACE_OUTER_BOUND('',#5198,.T.);
#3695=FACE_OUTER_BOUND('',#5199,.T.);
#3696=FACE_OUTER_BOUND('',#5200,.T.);
#3697=FACE_OUTER_BOUND('',#5201,.T.);
#3698=FACE_OUTER_BOUND('',#5202,.T.);
#3699=FACE_OUTER_BOUND('',#5203,.T.);
#3700=FACE_OUTER_BOUND('',#5204,.T.);
#3701=FACE_OUTER_BOUND('',#5205,.T.);
#3702=FACE_OUTER_BOUND('',#5208,.T.);
#5195=EDGE_LOOP('',(#19862,#19863,#19864,#19865));
#5196=EDGE_LOOP('',(#19866,#19867,#19868,#19869));
#5197=EDGE_LOOP('',(#19870,#19871,#19872,#19873));
#5198=EDGE_LOOP('',(#19874,#19875,#19876,#19877));
#5199=EDGE_LOOP('',(#19878,#19879,#19880,#19881));
#5200=EDGE_LOOP('',(#19882,#19883,#19884,#19885));
#5201=EDGE_LOOP('',(#19886,#19887,#19888,#19889));
#5202=EDGE_LOOP('',(#19890,#19891,#19892,#19893));
#5203=EDGE_LOOP('',(#19894,#19895,#19896,#19897));
#5204=EDGE_LOOP('',(#19898,#19899,#19900,#19901));
#5205=EDGE_LOOP('',(#19902,#19903,#19904,#19905,#19906,#19907,#19908,#19909));
#5206=EDGE_LOOP('',(#19910));
#5207=EDGE_LOOP('',(#19911));
#5208=EDGE_LOOP('',(#19912,#19913,#19914,#19915,#19916,#19917,#19918,#19919));
#5209=EDGE_LOOP('',(#19920));
#5210=EDGE_LOOP('',(#19921));
#6544=LINE('',#48515,#7977);
#6545=LINE('',#48521,#7978);
#6546=LINE('',#48526,#7979);
#6547=LINE('',#48528,#7980);
#6548=LINE('',#48530,#7981);
#6549=LINE('',#48531,#7982);
#6550=LINE('',#48537,#7983);
#6551=LINE('',#48540,#7984);
#6552=LINE('',#48542,#7985);
#6553=LINE('',#48543,#7986);
#6554=LINE('',#48549,#7987);
#6555=LINE('',#48552,#7988);
#6556=LINE('',#48554,#7989);
#6557=LINE('',#48555,#7990);
#6558=LINE('',#48561,#7991);
#6559=LINE('',#48564,#7992);
#6560=LINE('',#48566,#7993);
#6561=LINE('',#48567,#7994);
#7977=VECTOR('',#29358,0.1);
#7978=VECTOR('',#29365,0.1);
#7979=VECTOR('',#29370,1.);
#7980=VECTOR('',#29371,1.);
#7981=VECTOR('',#29372,1.);
#7982=VECTOR('',#29373,1.);
#7983=VECTOR('',#29380,1.);
#7984=VECTOR('',#29383,1.);
#7985=VECTOR('',#29384,1.);
#7986=VECTOR('',#29385,1.);
#7987=VECTOR('',#29392,1.);
#7988=VECTOR('',#29395,1.);
#7989=VECTOR('',#29396,1.);
#7990=VECTOR('',#29397,1.);
#7991=VECTOR('',#29404,1.);
#7992=VECTOR('',#29407,1.);
#7993=VECTOR('',#29408,1.);
#7994=VECTOR('',#29409,1.);
#9033=CIRCLE('',#24638,0.1);
#9034=CIRCLE('',#24639,0.1);
#9035=CIRCLE('',#24641,0.1);
#9036=CIRCLE('',#24642,0.1);
#9037=CIRCLE('',#24645,0.328820889047374);
#9038=CIRCLE('',#24646,0.328820889047374);
#9039=CIRCLE('',#24649,1.195);
#9040=CIRCLE('',#24650,1.195);
#9041=CIRCLE('',#24653,0.328820889047374);
#9042=CIRCLE('',#24654,0.328820889047374);
#9043=CIRCLE('',#24657,1.53);
#9044=CIRCLE('',#24658,1.53);
#10877=VERTEX_POINT('',#48512);
#10878=VERTEX_POINT('',#48514);
#10879=VERTEX_POINT('',#48518);
#10880=VERTEX_POINT('',#48520);
#10881=VERTEX_POINT('',#48524);
#10882=VERTEX_POINT('',#48525);
#10883=VERTEX_POINT('',#48527);
#10884=VERTEX_POINT('',#48529);
#10885=VERTEX_POINT('',#48533);
#10886=VERTEX_POINT('',#48535);
#10887=VERTEX_POINT('',#48539);
#10888=VERTEX_POINT('',#48541);
#10889=VERTEX_POINT('',#48545);
#10890=VERTEX_POINT('',#48547);
#10891=VERTEX_POINT('',#48551);
#10892=VERTEX_POINT('',#48553);
#10893=VERTEX_POINT('',#48557);
#10894=VERTEX_POINT('',#48559);
#10895=VERTEX_POINT('',#48563);
#10896=VERTEX_POINT('',#48565);
#13935=EDGE_CURVE('',#10877,#10877,#9033,.T.);
#13936=EDGE_CURVE('',#10877,#10878,#6544,.T.);
#13937=EDGE_CURVE('',#10878,#10878,#9034,.T.);
#13938=EDGE_CURVE('',#10879,#10879,#9035,.T.);
#13939=EDGE_CURVE('',#10879,#10880,#6545,.T.);
#13940=EDGE_CURVE('',#10880,#10880,#9036,.T.);
#13941=EDGE_CURVE('',#10881,#10882,#6546,.T.);
#13942=EDGE_CURVE('',#10881,#10883,#6547,.T.);
#13943=EDGE_CURVE('',#10884,#10883,#6548,.T.);
#13944=EDGE_CURVE('',#10882,#10884,#6549,.T.);
#13945=EDGE_CURVE('',#10885,#10882,#9037,.T.);
#13946=EDGE_CURVE('',#10886,#10884,#9038,.T.);
#13947=EDGE_CURVE('',#10885,#10886,#6550,.T.);
#13948=EDGE_CURVE('',#10885,#10887,#6551,.T.);
#13949=EDGE_CURVE('',#10888,#10886,#6552,.T.);
#13950=EDGE_CURVE('',#10887,#10888,#6553,.T.);
#13951=EDGE_CURVE('',#10887,#10889,#9039,.T.);
#13952=EDGE_CURVE('',#10890,#10888,#9040,.T.);
#13953=EDGE_CURVE('',#10889,#10890,#6554,.T.);
#13954=EDGE_CURVE('',#10889,#10891,#6555,.T.);
#13955=EDGE_CURVE('',#10892,#10890,#6556,.T.);
#13956=EDGE_CURVE('',#10891,#10892,#6557,.T.);
#13957=EDGE_CURVE('',#10893,#10891,#9041,.T.);
#13958=EDGE_CURVE('',#10894,#10892,#9042,.T.);
#13959=EDGE_CURVE('',#10893,#10894,#6558,.T.);
#13960=EDGE_CURVE('',#10893,#10895,#6559,.T.);
#13961=EDGE_CURVE('',#10896,#10894,#6560,.T.);
#13962=EDGE_CURVE('',#10895,#10896,#6561,.T.);
#13963=EDGE_CURVE('',#10881,#10895,#9043,.T.);
#13964=EDGE_CURVE('',#10883,#10896,#9044,.T.);
#19862=ORIENTED_EDGE('',*,*,#13935,.F.);
#19863=ORIENTED_EDGE('',*,*,#13936,.T.);
#19864=ORIENTED_EDGE('',*,*,#13937,.F.);
#19865=ORIENTED_EDGE('',*,*,#13936,.F.);
#19866=ORIENTED_EDGE('',*,*,#13938,.F.);
#19867=ORIENTED_EDGE('',*,*,#13939,.T.);
#19868=ORIENTED_EDGE('',*,*,#13940,.F.);
#19869=ORIENTED_EDGE('',*,*,#13939,.F.);
#19870=ORIENTED_EDGE('',*,*,#13941,.F.);
#19871=ORIENTED_EDGE('',*,*,#13942,.T.);
#19872=ORIENTED_EDGE('',*,*,#13943,.F.);
#19873=ORIENTED_EDGE('',*,*,#13944,.F.);
#19874=ORIENTED_EDGE('',*,*,#13945,.T.);
#19875=ORIENTED_EDGE('',*,*,#13944,.T.);
#19876=ORIENTED_EDGE('',*,*,#13946,.F.);
#19877=ORIENTED_EDGE('',*,*,#13947,.F.);
#19878=ORIENTED_EDGE('',*,*,#13948,.F.);
#19879=ORIENTED_EDGE('',*,*,#13947,.T.);
#19880=ORIENTED_EDGE('',*,*,#13949,.F.);
#19881=ORIENTED_EDGE('',*,*,#13950,.F.);
#19882=ORIENTED_EDGE('',*,*,#13951,.F.);
#19883=ORIENTED_EDGE('',*,*,#13950,.T.);
#19884=ORIENTED_EDGE('',*,*,#13952,.F.);
#19885=ORIENTED_EDGE('',*,*,#13953,.F.);
#19886=ORIENTED_EDGE('',*,*,#13954,.F.);
#19887=ORIENTED_EDGE('',*,*,#13953,.T.);
#19888=ORIENTED_EDGE('',*,*,#13955,.F.);
#19889=ORIENTED_EDGE('',*,*,#13956,.F.);
#19890=ORIENTED_EDGE('',*,*,#13957,.T.);
#19891=ORIENTED_EDGE('',*,*,#13956,.T.);
#19892=ORIENTED_EDGE('',*,*,#13958,.F.);
#19893=ORIENTED_EDGE('',*,*,#13959,.F.);
#19894=ORIENTED_EDGE('',*,*,#13960,.F.);
#19895=ORIENTED_EDGE('',*,*,#13959,.T.);
#19896=ORIENTED_EDGE('',*,*,#13961,.F.);
#19897=ORIENTED_EDGE('',*,*,#13962,.F.);
#19898=ORIENTED_EDGE('',*,*,#13963,.T.);
#19899=ORIENTED_EDGE('',*,*,#13962,.T.);
#19900=ORIENTED_EDGE('',*,*,#13964,.F.);
#19901=ORIENTED_EDGE('',*,*,#13942,.F.);
#19902=ORIENTED_EDGE('',*,*,#13964,.T.);
#19903=ORIENTED_EDGE('',*,*,#13961,.T.);
#19904=ORIENTED_EDGE('',*,*,#13958,.T.);
#19905=ORIENTED_EDGE('',*,*,#13955,.T.);
#19906=ORIENTED_EDGE('',*,*,#13952,.T.);
#19907=ORIENTED_EDGE('',*,*,#13949,.T.);
#19908=ORIENTED_EDGE('',*,*,#13946,.T.);
#19909=ORIENTED_EDGE('',*,*,#13943,.T.);
#19910=ORIENTED_EDGE('',*,*,#13935,.T.);
#19911=ORIENTED_EDGE('',*,*,#13938,.T.);
#19912=ORIENTED_EDGE('',*,*,#13963,.F.);
#19913=ORIENTED_EDGE('',*,*,#13941,.T.);
#19914=ORIENTED_EDGE('',*,*,#13945,.F.);
#19915=ORIENTED_EDGE('',*,*,#13948,.T.);
#19916=ORIENTED_EDGE('',*,*,#13951,.T.);
#19917=ORIENTED_EDGE('',*,*,#13954,.T.);
#19918=ORIENTED_EDGE('',*,*,#13957,.F.);
#19919=ORIENTED_EDGE('',*,*,#13960,.T.);
#19920=ORIENTED_EDGE('',*,*,#13937,.T.);
#19921=ORIENTED_EDGE('',*,*,#13940,.T.);
#22521=ADVANCED_FACE('',(#3691),#2583,.F.);
#22522=ADVANCED_FACE('',(#3692),#2584,.F.);
#22523=ADVANCED_FACE('',(#3693),#2232,.T.);
#22524=ADVANCED_FACE('',(#3694),#2585,.T.);
#22525=ADVANCED_FACE('',(#3695),#2233,.T.);
#22526=ADVANCED_FACE('',(#3696),#2586,.F.);
#22527=ADVANCED_FACE('',(#3697),#2234,.T.);
#22528=ADVANCED_FACE('',(#3698),#2587,.T.);
#22529=ADVANCED_FACE('',(#3699),#2235,.T.);
#22530=ADVANCED_FACE('',(#3700),#2588,.T.);
#22531=ADVANCED_FACE('',(#3701,#1798,#1799),#2236,.T.);
#22532=ADVANCED_FACE('',(#3702,#1800,#1801),#2237,.F.);
#22821=CLOSED_SHELL('',(#22521,#22522,#22523,#22524,#22525,#22526,#22527,
#22528,#22529,#22530,#22531,#22532));
#24636=AXIS2_PLACEMENT_3D('',#48510,#29352,#29353);
#24637=AXIS2_PLACEMENT_3D('',#48511,#29354,#29355);
#24638=AXIS2_PLACEMENT_3D('',#48513,#29356,#29357);
#24639=AXIS2_PLACEMENT_3D('',#48516,#29359,#29360);
#24640=AXIS2_PLACEMENT_3D('',#48517,#29361,#29362);
#24641=AXIS2_PLACEMENT_3D('',#48519,#29363,#29364);
#24642=AXIS2_PLACEMENT_3D('',#48522,#29366,#29367);
#24643=AXIS2_PLACEMENT_3D('',#48523,#29368,#29369);
#24644=AXIS2_PLACEMENT_3D('',#48532,#29374,#29375);
#24645=AXIS2_PLACEMENT_3D('',#48534,#29376,#29377);
#24646=AXIS2_PLACEMENT_3D('',#48536,#29378,#29379);
#24647=AXIS2_PLACEMENT_3D('',#48538,#29381,#29382);
#24648=AXIS2_PLACEMENT_3D('',#48544,#29386,#29387);
#24649=AXIS2_PLACEMENT_3D('',#48546,#29388,#29389);
#24650=AXIS2_PLACEMENT_3D('',#48548,#29390,#29391);
#24651=AXIS2_PLACEMENT_3D('',#48550,#29393,#29394);
#24652=AXIS2_PLACEMENT_3D('',#48556,#29398,#29399);
#24653=AXIS2_PLACEMENT_3D('',#48558,#29400,#29401);
#24654=AXIS2_PLACEMENT_3D('',#48560,#29402,#29403);
#24655=AXIS2_PLACEMENT_3D('',#48562,#29405,#29406);
#24656=AXIS2_PLACEMENT_3D('',#48568,#29410,#29411);
#24657=AXIS2_PLACEMENT_3D('',#48569,#29412,#29413);
#24658=AXIS2_PLACEMENT_3D('',#48570,#29414,#29415);
#24659=AXIS2_PLACEMENT_3D('',#48571,#29416,#29417);
#24660=AXIS2_PLACEMENT_3D('',#48572,#29418,#29419);
#29352=DIRECTION('axis',(0.,0.,1.));
#29353=DIRECTION('refdir',(1.,0.,0.));
#29354=DIRECTION('center_axis',(0.,0.,-1.));
#29355=DIRECTION('ref_axis',(1.,0.,0.));
#29356=DIRECTION('center_axis',(0.,0.,-1.));
#29357=DIRECTION('ref_axis',(1.,0.,0.));
#29358=DIRECTION('',(0.,0.,-1.));
#29359=DIRECTION('center_axis',(0.,0.,1.));
#29360=DIRECTION('ref_axis',(1.,0.,0.));
#29361=DIRECTION('center_axis',(0.,0.,-1.));
#29362=DIRECTION('ref_axis',(1.,0.,0.));
#29363=DIRECTION('center_axis',(0.,0.,-1.));
#29364=DIRECTION('ref_axis',(1.,0.,0.));
#29365=DIRECTION('',(0.,0.,-1.));
#29366=DIRECTION('center_axis',(0.,0.,1.));
#29367=DIRECTION('ref_axis',(1.,0.,0.));
#29368=DIRECTION('center_axis',(0.529919264233205,-0.848048096156426,0.));
#29369=DIRECTION('ref_axis',(0.848048096156426,0.529919264233205,0.));
#29370=DIRECTION('',(-0.848048096156426,-0.529919264233205,0.));
#29371=DIRECTION('',(0.,0.,1.));
#29372=DIRECTION('',(0.848048096156426,0.529919264233205,0.));
#29373=DIRECTION('',(0.,0.,1.));
#29374=DIRECTION('center_axis',(0.,0.,1.));
#29375=DIRECTION('ref_axis',(-0.8811002033343,0.472929626566422,0.));
#29376=DIRECTION('center_axis',(0.,0.,1.));
#29377=DIRECTION('ref_axis',(-0.8811002033343,0.472929626566422,0.));
#29378=DIRECTION('center_axis',(0.,0.,1.));
#29379=DIRECTION('ref_axis',(-0.8811002033343,0.472929626566422,0.));
#29380=DIRECTION('',(0.,0.,1.));
#29381=DIRECTION('center_axis',(-0.241921895599668,0.970295726275997,0.));
#29382=DIRECTION('ref_axis',(-0.970295726275997,-0.241921895599668,0.));
#29383=DIRECTION('',(0.970295726275997,0.241921895599668,0.));
#29384=DIRECTION('',(-0.970295726275997,-0.241921895599668,0.));
#29385=DIRECTION('',(0.,0.,1.));
#29386=DIRECTION('center_axis',(0.,0.,1.));
#29387=DIRECTION('ref_axis',(1.,-4.64528462186258E-17,0.));
#29388=DIRECTION('center_axis',(0.,0.,1.));
#29389=DIRECTION('ref_axis',(-0.970295726275996,-0.241921895599668,0.));
#29390=DIRECTION('center_axis',(0.,0.,-1.));
#29391=DIRECTION('ref_axis',(-0.970295726275996,-0.241921895599668,0.));
#29392=DIRECTION('',(0.,0.,1.));
#29393=DIRECTION('center_axis',(-0.241921895599668,-0.970295726275996,0.));
#29394=DIRECTION('ref_axis',(0.970295726275996,-0.241921895599668,0.));
#29395=DIRECTION('',(-0.970295726275996,0.241921895599668,0.));
#29396=DIRECTION('',(0.970295726275996,-0.241921895599668,0.));
#29397=DIRECTION('',(0.,0.,1.));
#29398=DIRECTION('center_axis',(0.,0.,1.));
#29399=DIRECTION('ref_axis',(-0.060878153376398,0.998145205088658,0.));
#29400=DIRECTION('center_axis',(0.,0.,1.));
#29401=DIRECTION('ref_axis',(-0.060878153376398,0.998145205088658,0.));
#29402=DIRECTION('center_axis',(0.,0.,1.));
#29403=DIRECTION('ref_axis',(-0.060878153376398,0.998145205088658,0.));
#29404=DIRECTION('',(0.,0.,1.));
#29405=DIRECTION('center_axis',(0.529919264233205,0.848048096156426,0.));
#29406=DIRECTION('ref_axis',(-0.848048096156426,0.529919264233205,0.));
#29407=DIRECTION('',(0.848048096156426,-0.529919264233205,0.));
#29408=DIRECTION('',(-0.848048096156426,0.529919264233205,0.));
#29409=DIRECTION('',(0.,0.,1.));
#29410=DIRECTION('center_axis',(0.,0.,1.));
#29411=DIRECTION('ref_axis',(1.,-1.45127192761458E-16,0.));
#29412=DIRECTION('center_axis',(0.,0.,1.));
#29413=DIRECTION('ref_axis',(-0.848048096156426,-0.529919264233205,0.));
#29414=DIRECTION('center_axis',(0.,0.,1.));
#29415=DIRECTION('ref_axis',(-0.848048096156426,-0.529919264233205,0.));
#29416=DIRECTION('center_axis',(0.,0.,1.));
#29417=DIRECTION('ref_axis',(1.,0.,0.));
#29418=DIRECTION('center_axis',(0.,0.,1.));
#29419=DIRECTION('ref_axis',(1.,0.,0.));
#48510=CARTESIAN_POINT('',(0.,0.,0.));
#48511=CARTESIAN_POINT('Origin',(-1.43138504711854,-0.60758690480082,0.12));
#48512=CARTESIAN_POINT('',(-1.53138504711854,-0.60758690480082,0.12));
#48513=CARTESIAN_POINT('Origin',(-1.43138504711854,-0.60758690480082,0.12));
#48514=CARTESIAN_POINT('',(-1.53138504711854,-0.60758690480082,0.));
#48515=CARTESIAN_POINT('',(-1.53138504711854,-0.60758690480082,0.12));
#48516=CARTESIAN_POINT('Origin',(-1.43138504711854,-0.60758690480082,0.));
#48517=CARTESIAN_POINT('Origin',(-1.43138504711854,0.607586904800821,0.12));
#48518=CARTESIAN_POINT('',(-1.53138504711854,0.607586904800821,0.12));
#48519=CARTESIAN_POINT('Origin',(-1.43138504711854,0.607586904800821,0.12));
#48520=CARTESIAN_POINT('',(-1.53138504711854,0.607586904800821,0.));
#48521=CARTESIAN_POINT('',(-1.53138504711854,0.607586904800821,0.12));
#48522=CARTESIAN_POINT('Origin',(-1.43138504711854,0.607586904800821,0.));
#48523=CARTESIAN_POINT('Origin',(-1.46712320635062,-0.916760327123444,0.));
#48524=CARTESIAN_POINT('',(-1.29751358711933,-0.810776474276803,0.));
#48525=CARTESIAN_POINT('',(-1.46712320635062,-0.916760327123444,0.));
#48526=CARTESIAN_POINT('',(-1.29751358711933,-0.810776474276803,0.));
#48527=CARTESIAN_POINT('',(-1.29751358711933,-0.810776474276803,0.12));
#48528=CARTESIAN_POINT('',(-1.29751358711933,-0.810776474276803,0.));
#48529=CARTESIAN_POINT('',(-1.46712320635062,-0.916760327123444,0.12));
#48530=CARTESIAN_POINT('',(-1.29751358711933,-0.810776474276803,0.12));
#48531=CARTESIAN_POINT('',(-1.46712320635062,-0.916760327123444,0.));
#48532=CARTESIAN_POINT('Origin',(-1.44710519783383,-0.588549333387818,0.));
#48533=CARTESIAN_POINT('',(-1.73682935003403,-0.433040193123405,0.));
#48534=CARTESIAN_POINT('Origin',(-1.44710519783383,-0.588549333387818,0.));
#48535=CARTESIAN_POINT('',(-1.73682935003403,-0.433040193123405,0.12));
#48536=CARTESIAN_POINT('Origin',(-1.44710519783383,-0.588549333387818,0.12));
#48537=CARTESIAN_POINT('',(-1.73682935003403,-0.433040193123405,0.));
#48538=CARTESIAN_POINT('Origin',(-1.15950339289982,-0.289096665241603,0.));
#48539=CARTESIAN_POINT('',(-1.15950339289982,-0.289096665241603,0.));
#48540=CARTESIAN_POINT('',(-1.73682935003403,-0.433040193123405,0.));
#48541=CARTESIAN_POINT('',(-1.15950339289982,-0.289096665241603,0.12));
#48542=CARTESIAN_POINT('',(-1.73682935003403,-0.433040193123405,0.12));
#48543=CARTESIAN_POINT('',(-1.15950339289982,-0.289096665241603,0.));
#48544=CARTESIAN_POINT('Origin',(-4.16333634234434E-17,1.38777878078145E-16,
0.));
#48545=CARTESIAN_POINT('',(-1.15950339289982,0.289096665241603,0.));
#48546=CARTESIAN_POINT('Origin',(-4.16333634234434E-17,1.38777878078145E-16,
0.));
#48547=CARTESIAN_POINT('',(-1.15950339289982,0.289096665241603,0.12));
#48548=CARTESIAN_POINT('Origin',(-4.16333634234434E-17,1.38777878078145E-16,
0.12));
#48549=CARTESIAN_POINT('',(-1.15950339289982,0.289096665241603,0.));
#48550=CARTESIAN_POINT('Origin',(-1.73682935003403,0.433040193123405,0.));
#48551=CARTESIAN_POINT('',(-1.73682935003403,0.433040193123405,0.));
#48552=CARTESIAN_POINT('',(-1.15950339289982,0.289096665241603,0.));
#48553=CARTESIAN_POINT('',(-1.73682935003403,0.433040193123405,0.12));
#48554=CARTESIAN_POINT('',(-1.15950339289982,0.289096665241603,0.12));
#48555=CARTESIAN_POINT('',(-1.73682935003403,0.433040193123405,0.));
#48556=CARTESIAN_POINT('Origin',(-1.44710519783383,0.588549333387818,0.));
#48557=CARTESIAN_POINT('',(-1.46712320635062,0.916760327123444,0.));
#48558=CARTESIAN_POINT('Origin',(-1.44710519783383,0.588549333387818,0.));
#48559=CARTESIAN_POINT('',(-1.46712320635062,0.916760327123444,0.12));
#48560=CARTESIAN_POINT('Origin',(-1.44710519783383,0.588549333387818,0.12));
#48561=CARTESIAN_POINT('',(-1.46712320635062,0.916760327123444,0.));
#48562=CARTESIAN_POINT('Origin',(-1.29751358711933,0.810776474276804,0.));
#48563=CARTESIAN_POINT('',(-1.29751358711933,0.810776474276804,0.));
#48564=CARTESIAN_POINT('',(-1.46712320635062,0.916760327123444,0.));
#48565=CARTESIAN_POINT('',(-1.29751358711933,0.810776474276804,0.12));
#48566=CARTESIAN_POINT('',(-1.46712320635062,0.916760327123444,0.12));
#48567=CARTESIAN_POINT('',(-1.29751358711933,0.810776474276804,0.));
#48568=CARTESIAN_POINT('Origin',(5.55111512312578E-17,-2.77555756156289E-16,
0.));
#48569=CARTESIAN_POINT('Origin',(5.55111512312578E-17,-2.77555756156289E-16,
0.));
#48570=CARTESIAN_POINT('Origin',(5.55111512312578E-17,-2.77555756156289E-16,
0.12));
#48571=CARTESIAN_POINT('Origin',(-0.122963043440601,-2.22044604925031E-16,
0.12));
#48572=CARTESIAN_POINT('Origin',(-0.122963043440601,-2.22044604925031E-16,
0.));
#59179=UNCERTAINTY_MEASURE_WITH_UNIT(LENGTH_MEASURE(0.001),#59205,
'DISTANCE_ACCURACY_VALUE',
'Maximum model space distance between geometric entities at asserted c
onnectivities');
#59182=UNCERTAINTY_MEASURE_WITH_UNIT(LENGTH_MEASURE(0.001),#59205,
'DISTANCE_ACCURACY_VALUE',
'Maximum model space distance between geometric entities at asserted c
onnectivities');
#59201=(
GEOMETRIC_REPRESENTATION_CONTEXT(3)
GLOBAL_UNCERTAINTY_ASSIGNED_CONTEXT((#59179))
GLOBAL_UNIT_ASSIGNED_CONTEXT((#59205,#59207,#59208))
REPRESENTATION_CONTEXT('','3D')
);
#59204=(
GEOMETRIC_REPRESENTATION_CONTEXT(3)
GLOBAL_UNCERTAINTY_ASSIGNED_CONTEXT((#59182))
GLOBAL_UNIT_ASSIGNED_CONTEXT((#59205,#59207,#59208))
REPRESENTATION_CONTEXT('','3D')
);
#59205=(
LENGTH_UNIT()
NAMED_UNIT(*)
SI_UNIT(.CENTI.,.METRE.)
);
#59207=(
NAMED_UNIT(*)
PLANE_ANGLE_UNIT()
SI_UNIT($,.RADIAN.)
);
#59208=(
NAMED_UNIT(*)
SI_UNIT($,.STERADIAN.)
SOLID_ANGLE_UNIT()
);
#59227=SHAPE_DEFINITION_REPRESENTATION(#59248,#59314);
#59248=PRODUCT_DEFINITION_SHAPE('',$,#59336);
#59314=SHAPE_REPRESENTATION('',(#24636),#59201);
#59317=PRODUCT_DEFINITION_CONTEXT('part definition',#59382,'design');
#59336=PRODUCT_DEFINITION('2026-10-23-00-47-22-382',
'15_DIN_471_25x1.2_Retaining_Ring',#59357,#59317);
#59357=PRODUCT_DEFINITION_FORMATION('',$,#59402);
#59382=APPLICATION_CONTEXT(
'Core Data for Automotive Mechanical Design Process');
#59383=PRODUCT_CONTEXT('part definition',#59382,'mechanical');
#59402=PRODUCT('2026-10-23-00-47-22-382',
'15_DIN_471_25x1.2_Retaining_Ring',$,(#59383));
#59594=COLOUR_RGB('Off White',0.89,0.88,0.83);
#59595=FILL_AREA_STYLE_COLOUR('',#59594);
#59596=FILL_AREA_STYLE('',(#59595));
#59597=SURFACE_STYLE_FILL_AREA(#59596);
#59598=SURFACE_SIDE_STYLE('',(#59597));
#59599=SURFACE_STYLE_USAGE(.BOTH.,#59598);
#59600=PRESENTATION_STYLE_ASSIGNMENT((#59599));
ENDSEC;
END-ISO-10303-21;
